ISO-10303-21;
HEADER;
FILE_DESCRIPTION (('STEP AP203'),
    '1' );
FILE_NAME ('1602p_c_15.step',
    '2026-10-31T14:11:27',
    ( '' ),
    ( '' ),
    'SwSTEP 2.0',
    'SolidWorks 2024',
    '' );
FILE_SCHEMA (( 'AUTOMOTIVE_DESIGN' ));
ENDSEC;

DATA;
#332=PLANE ( 'NONE',  #10040 ) ;
#415=DIRECTION ( 'NONE',  ( 1.000000000000000000, 0.000000000000000000, 0.000000000000000000 ) ) ;
#475=VECTOR ( 'NONE', #6240, 1000.000000000000000 ) ;
#899=FACE_OUTER_BOUND ( 'NONE', #15070, .T. ) ;
#2039=CARTESIAN_POINT ( 'NONE',  ( -19.55420733641118147, 2.397309549614596857, 4.999999999999993783 ) ) ;
#2243=DIRECTION ( 'NONE',  ( 2.874764335373299684E-17, -2.286959927910970108E-15, -1.000000000000000000 ) ) ;
#2334=DIRECTION ( 'NONE',  ( 3.211814849206744928E-17, -2.442368445299930211E-15, -1.000000000000000000 ) ) ;
#2447=PLANE ( 'NONE',  #13761 ) ;
#2569=CARTESIAN_POINT ( 'NONE',  ( 0.000000000000000000, 0.000000000000000000, 0.000000000000000000 ) ) ;
#3082=ORIENTED_EDGE ( 'NONE', *, *, #8388, .F. ) ;
#3368=ORIENTED_EDGE ( 'NONE', *, *, #23171, .T. ) ;
#3626=DIRECTION ( 'NONE',  ( 3.211814849206744928E-17, -2.442368445299930211E-15, -1.000000000000000000 ) ) ;
#3642=( GEOMETRIC_REPRESENTATION_CONTEXT ( 3 ) GLOBAL_UNCERTAINTY_ASSIGNED_CONTEXT ( ( #17195 ) ) GLOBAL_UNIT_ASSIGNED_CONTEXT ( ( #14656, #4084, #20245 ) ) REPRESENTATION_CONTEXT ( 'NONE', 'WORKASPACE' ) );
#4062=CARTESIAN_POINT ( 'NONE',  ( -19.55420733641118147, 2.397309549614573765, -5.000000000000006217 ) ) ;
#4084=( NAMED_UNIT ( * ) PLANE_ANGLE_UNIT ( ) SI_UNIT ( $, .RADIAN. ) );
#4086=EDGE_CURVE ( 'NONE', #9241, #12615, #15253, .T. ) ;
#4100=DIRECTION ( 'NONE',  ( -6.574470837186350421E-32, 2.286959927910970108E-15, 1.000000000000000000 ) ) ;
#4144=EDGE_LOOP ( 'NONE', ( #15314, #21126, #15377, #16738 ) ) ;
#4191=DIRECTION ( 'NONE',  ( 3.211814849206744928E-17, -2.442368445299930211E-15, -1.000000000000000000 ) ) ;
#4215=AXIS2_PLACEMENT_3D ( 'NONE', #20256, #3626, #10899 ) ;
#4502=CLOSED_SHELL ( 'NONE', ( #8642, #6172, #17626, #18838 ) ) ;
#4514=SHAPE_DEFINITION_REPRESENTATION ( #18207, #13540 ) ;
#4574=APPLICATION_CONTEXT ( 'configuration controlled 3d designs of mechanical parts and assemblies' ) ;
#4728=PRODUCT ( '1602p_c_15', '1602p_c_15', '', ( #14510 ) ) ;
#5475=ORIENTED_EDGE ( 'NONE', *, *, #12471, .F. ) ;
#5604=CIRCLE ( 'NONE', #18901, 2.499999999999999112 ) ;
#5724=ORIENTED_EDGE ( 'NONE', *, *, #10517, .T. ) ;
#5902=CYLINDRICAL_SURFACE ( 'NONE', #22513, 2.499999999999999112 ) ;
#6172=ADVANCED_FACE ( 'NONE', ( #13227 ), #20460, .T. ) ;
#6231=DIRECTION ( 'NONE',  ( -0.02168293463503252055, 0.9997648975362223300, -2.428612866367530721E-15 ) ) ;
#6240=DIRECTION ( 'NONE',  ( 3.211814849206744928E-17, -2.442368445299930605E-15, -1.000000000000000000 ) ) ;
#6624=DIRECTION ( 'NONE',  ( 3.211814849206744928E-17, -2.442368445299930605E-15, -1.000000000000000000 ) ) ;
#6849=DESIGN_CONTEXT ( 'detailed design', #18712, 'design' ) ;
#7598=CARTESIAN_POINT ( 'NONE',  ( -19.52710366811739817, 1.147603427694289913, -5.000000000000000000 ) ) ;
#7746=ORIENTED_EDGE ( 'NONE', *, *, #4086, .T. ) ;
#7846=ORIENTED_EDGE ( 'NONE', *, *, #12471, .T. ) ;
#8388=EDGE_CURVE ( 'NONE', #9241, #21232, #11546, .T. ) ;
#8642=ADVANCED_FACE ( 'NONE', ( #899 ), #5902, .T. ) ;
#9241=VERTEX_POINT ( 'NONE', #15010 ) ;
#9448=MANIFOLD_SOLID_BREP ( 'Imported1', #4502 ) ;
#9704=CIRCLE ( 'NONE', #17271, 2.499999999999999112 ) ;
#10040=AXIS2_PLACEMENT_3D ( 'NONE', #7598, #2243, #16386 ) ;
#10349=PRODUCT_DEFINITION_FORMATION_WITH_SPECIFIED_SOURCE ( 'ANY', '', #4728, .NOT_KNOWN. ) ;
#10403=EDGE_CURVE ( 'NONE', #21232, #11204, #17419, .T. ) ;
#10517=EDGE_CURVE ( 'NONE', #12615, #11204, #12150, .T. ) ;
#10899=DIRECTION ( 'NONE',  ( -0.02168293463503252055, 0.9997648975362223300, -2.428612866367530721E-15 ) ) ;
#11204=VERTEX_POINT ( 'NONE', #4062 ) ;
#11546=CIRCLE ( 'NONE', #12666, 2.499999999999999112 ) ;
#12150=CIRCLE ( 'NONE', #4215, 2.499999999999999112 ) ;
#12471=EDGE_CURVE ( 'NONE', #21232, #9241, #5604, .T. ) ;
#12615=VERTEX_POINT ( 'NONE', #22947 ) ;
#12666=AXIS2_PLACEMENT_3D ( 'NONE', #21808, #12906, #20279 ) ;
#12739=AXIS2_PLACEMENT_3D ( 'NONE', #2569, #13380, #415 ) ;
#12906=DIRECTION ( 'NONE',  ( 3.211814849206744928E-17, -2.442368445299930211E-15, -1.000000000000000000 ) ) ;
#13227=FACE_OUTER_BOUND ( 'NONE', #4144, .T. ) ;
#13380=DIRECTION ( 'NONE',  ( 0.000000000000000000, 0.000000000000000000, 1.000000000000000000 ) ) ;
#13540=SHAPE_REPRESENTATION ( '1602p_c_15', ( #12739 ), #3642 ) ;
#13636=AXIS2_PLACEMENT_3D ( 'NONE', #17131, #4191, #18699 ) ;
#13761=AXIS2_PLACEMENT_3D ( 'NONE', #22250, #4100, #22504 ) ;
#14455=ADVANCED_BREP_SHAPE_REPRESENTATION ( '', ( #9448, #12739 ), #3642 ) ;
#14510=MECHANICAL_CONTEXT ( 'NONE', #4574, 'mechanical' ) ;
#14656=( LENGTH_UNIT ( ) NAMED_UNIT ( * ) SI_UNIT ( .MILLI., .METRE. ) );
#15010=CARTESIAN_POINT ( 'NONE',  ( -19.44579266323601985, -2.601514938066513682, 5.000000000000006217 ) ) ;
#15070=EDGE_LOOP ( 'NONE', ( #7846, #7746, #20375, #16136 ) ) ;
#15119=DIRECTION ( 'NONE',  ( 3.211814849206744928E-17, -2.442368445299930211E-15, -1.000000000000000000 ) ) ;
#15253=LINE ( 'NONE', #22499, #475 ) ;
#15275=CARTESIAN_POINT ( 'NONE',  ( -19.49999999982360066, -0.1021026942259749964, -2.500000000000000000 ) ) ;
#15314=ORIENTED_EDGE ( 'NONE', *, *, #4086, .F. ) ;
#15377=ORIENTED_EDGE ( 'NONE', *, *, #10403, .T. ) ;
#15459=PRODUCT_DEFINITION ( 'UNKNOWN', '', #10349, #6849 ) ;
#16136=ORIENTED_EDGE ( 'NONE', *, *, #10403, .F. ) ;
#16386=DIRECTION ( 'NONE',  ( 0.000000000000000000, -1.000000000000000000, 2.286959927910970108E-15 ) ) ;
#16608=FACE_OUTER_BOUND ( 'NONE', #18017, .T. ) ;
#16738=ORIENTED_EDGE ( 'NONE', *, *, #10517, .F. ) ;
#17131=CARTESIAN_POINT ( 'NONE',  ( -19.49999999982360066, -0.1021026942259749964, -2.500000000000000000 ) ) ;
#17195=UNCERTAINTY_MEASURE_WITH_UNIT (LENGTH_MEASURE( 1.000000000000000082E-05 ), #14656, 'distance_accuracy_value', 'NONE');
#17271=AXIS2_PLACEMENT_3D ( 'NONE', #22998, #19331, #21219 ) ;
#17419=LINE ( 'NONE', #22874, #21283 ) ;
#17626=ADVANCED_FACE ( 'NONE', ( #16608 ), #332, .T. ) ;
#18017=EDGE_LOOP ( 'NONE', ( #3368, #5724 ) ) ;
#18207=PRODUCT_DEFINITION_SHAPE ( 'NONE', 'NONE',  #15459 ) ;
#18699=DIRECTION ( 'NONE',  ( -0.02168293463503252055, 0.9997648975362223300, -2.428612866367530721E-15 ) ) ;
#18712=APPLICATION_CONTEXT ( 'configuration controlled 3d designs of mechanical parts and assemblies' ) ;
#18733=FACE_OUTER_BOUND ( 'NONE', #20861, .T. ) ;
#18826=CARTESIAN_POINT ( 'NONE',  ( -19.49999999982360066, -0.1021026942259579962, 5.000000000000000000 ) ) ;
#18838=ADVANCED_FACE ( 'NONE', ( #18733 ), #2447, .T. ) ;
#18901=AXIS2_PLACEMENT_3D ( 'NONE', #18826, #15119, #6231 ) ;
#19088=DIRECTION ( 'NONE',  ( -0.02168293463503252055, 0.9997648975362223300, -2.428612866367530721E-15 ) ) ;
#19331=DIRECTION ( 'NONE',  ( 3.211814849206744928E-17, -2.442368445299930211E-15, -1.000000000000000000 ) ) ;
#20245=( NAMED_UNIT ( * ) SI_UNIT ( $, .STERADIAN. ) SOLID_ANGLE_UNIT ( ) );
#20256=CARTESIAN_POINT ( 'NONE',  ( -19.49999999982360066, -0.1021026942259809916, -5.000000000000000000 ) ) ;
#20279=DIRECTION ( 'NONE',  ( -0.02168293463503252055, 0.9997648975362223300, -2.428612866367530721E-15 ) ) ;
#20375=ORIENTED_EDGE ( 'NONE', *, *, #23171, .F. ) ;
#20460=CYLINDRICAL_SURFACE ( 'NONE', #13636, 2.499999999999999112 ) ;
#20861=EDGE_LOOP ( 'NONE', ( #5475, #3082 ) ) ;
#21126=ORIENTED_EDGE ( 'NONE', *, *, #8388, .T. ) ;
#21219=DIRECTION ( 'NONE',  ( -0.02168293463503252055, 0.9997648975362223300, -2.428612866367530721E-15 ) ) ;
#21232=VERTEX_POINT ( 'NONE', #2039 ) ;
#21283=VECTOR ( 'NONE', #6624, 1000.000000000000000 ) ;
#21808=CARTESIAN_POINT ( 'NONE',  ( -19.49999999982360066, -0.1021026942259579962, 5.000000000000000000 ) ) ;
#21891=SHAPE_REPRESENTATION_RELATIONSHIP ( 'NONE' , 'NONE' ,  #13540, #14455 ) ;
#22250=CARTESIAN_POINT ( 'NONE',  ( -19.52710366811739817, 1.147603427694330103, 5.000000000000000000 ) ) ;
#22499=CARTESIAN_POINT ( 'NONE',  ( -19.44579266323601985, -2.601514938066530114, -2.499999999999993783 ) ) ;
#22504=DIRECTION ( 'NONE',  ( 1.000000000000000000, 2.874764335373299684E-17, 8.758115402030109610E-48 ) ) ;
#22513=AXIS2_PLACEMENT_3D ( 'NONE', #15275, #2334, #19088 ) ;
#22874=CARTESIAN_POINT ( 'NONE',  ( -19.55420733641118147, 2.397309549614579982, -2.500000000000006217 ) ) ;
#22947=CARTESIAN_POINT ( 'NONE',  ( -19.44579266323601985, -2.601514938066536331, -4.999999999999993783 ) ) ;
#22998=CARTESIAN_POINT ( 'NONE',  ( -19.49999999982360066, -0.1021026942259809916, -5.000000000000000000 ) ) ;
#23171=EDGE_CURVE ( 'NONE', #11204, #12615, #9704, .T. ) ;
#23550=COLOUR_RGB('Black', 0.08235294, 0.09019608, 0.10196078);
#23551=FILL_AREA_STYLE_COLOUR('',#23550);
#23552=FILL_AREA_STYLE('',(#23551));
#23553=SURFACE_STYLE_FILL_AREA(#23552);
#23554=SURFACE_SIDE_STYLE('',(#23553));
#23555=SURFACE_STYLE_USAGE(.BOTH.,#23554);
#23556=PRESENTATION_STYLE_ASSIGNMENT((#23555));
#23601=STYLED_ITEM('',(#23556),#9448);
#23602=MECHANICAL_DESIGN_GEOMETRIC_PRESENTATION_REPRESENTATION('',(#23601),#3642);
ENDSEC;
END-ISO-10303-21;
